ISO-10303-21;
HEADER;
/* Generated by software containing ST-Developer
 * from STEP Tools, Inc. (www.steptools.com) 
 */

FILE_DESCRIPTION(
/* description */ ('Hand-crank gear train demonstrator'),
/* implementation_level */ '2;1');

FILE_NAME(
/* name */ 'Socket Set Screw - M5x8.step',
/* time_stamp */ '2026-10-28T03:22:13-07:00',
/* author */ (''),
/* organization */ (''),
/* preprocessor_version */ 'ST-DEVELOPER v20.2',
/* originating_system */ 'Autodesk Translation Framework v15.17.0.0',
/* authorisation */ '');

FILE_SCHEMA (('AUTOMOTIVE_DESIGN { 1 0 10303 214 3 1 1 }'));
ENDSEC;

DATA;
#10=MECHANICAL_DESIGN_GEOMETRIC_PRESENTATION_REPRESENTATION('',(#1265),#62758);
#1045=CONICAL_SURFACE('',#18676,0.235,0.785398163397448);
#1046=CONICAL_SURFACE('',#18680,0.2125,0.785398163397448);
#1122=SHAPE_REPRESENTATION_RELATIONSHIP('SRR','None',#63100,#1186);
#1186=ADVANCED_BREP_SHAPE_REPRESENTATION('',(#1340),#62754);
#1265=STYLED_ITEM('',(#63469),#1340);
#1340=MANIFOLD_SOLID_BREP('Body1',#16449);
#1629=FACE_BOUND('',#4257,.T.);
#2101=PLANE('',#18667);
#2102=PLANE('',#18668);
#2103=PLANE('',#18669);
#2104=PLANE('',#18670);
#2105=PLANE('',#18671);
#2106=PLANE('',#18672);
#2107=PLANE('',#18673);
#2108=PLANE('',#18674);
#2109=PLANE('',#18682);
#3026=FACE_OUTER_BOUND('',#4249,.T.);
#3027=FACE_OUTER_BOUND('',#4250,.T.);
#3028=FACE_OUTER_BOUND('',#4251,.T.);
#3029=FACE_OUTER_BOUND('',#4252,.T.);
#3030=FACE_OUTER_BOUND('',#4253,.T.);
#3031=FACE_OUTER_BOUND('',#4254,.T.);
#3032=FACE_OUTER_BOUND('',#4255,.T.);
#3033=FACE_OUTER_BOUND('',#4256,.T.);
#3034=FACE_OUTER_BOUND('',#4258,.T.);
#3035=FACE_OUTER_BOUND('',#4259,.T.);
#3036=FACE_OUTER_BOUND('',#4260,.T.);
#3037=FACE_OUTER_BOUND('',#4261,.T.);
#4249=EDGE_LOOP('',(#15041,#15042,#15043,#15044));
#4250=EDGE_LOOP('',(#15045,#15046,#15047,#15048));
#4251=EDGE_LOOP('',(#15049,#15050,#15051,#15052));
#4252=EDGE_LOOP('',(#15053,#15054,#15055,#15056));
#4253=EDGE_LOOP('',(#15057,#15058,#15059,#15060));
#4254=EDGE_LOOP('',(#15061,#15062,#15063,#15064));
#4255=EDGE_LOOP('',(#15065,#15066,#15067,#15068,#15069,#15070));
#4256=EDGE_LOOP('',(#15071));
#4257=EDGE_LOOP('',(#15072,#15073,#15074,#15075,#15076,#15077));
#4258=EDGE_LOOP('',(#15078,#15079,#15080,#15081));
#4259=EDGE_LOOP('',(#15082,#15083,#15084,#15085));
#4260=EDGE_LOOP('',(#15086,#15087,#15088,#15089));
#4261=EDGE_LOOP('',(#15090));
#5371=LINE('',#62363,#6503);
#5372=LINE('',#62365,#6504);
#5373=LINE('',#62367,#6505);
#5374=LINE('',#62368,#6506);
#5375=LINE('',#62371,#6507);
#5376=LINE('',#62373,#6508);
#5377=LINE('',#62374,#6509);
#5378=LINE('',#62377,#6510);
#5379=LINE('',#62379,#6511);
#5380=LINE('',#62380,#6512);
#5381=LINE('',#62383,#6513);
#5382=LINE('',#62385,#6514);
#5383=LINE('',#62386,#6515);
#5384=LINE('',#62389,#6516);
#5385=LINE('',#62391,#6517);
#5386=LINE('',#62392,#6518);
#5387=LINE('',#62394,#6519);
#5388=LINE('',#62395,#6520);
#5389=LINE('',#62403,#6521);
#5390=LINE('',#62407,#6522);
#5391=LINE('',#62411,#6523);
#6503=VECTOR('',#22936,1.);
#6504=VECTOR('',#22937,1.);
#6505=VECTOR('',#22938,1.);
#6506=VECTOR('',#22939,1.);
#6507=VECTOR('',#22942,1.);
#6508=VECTOR('',#22943,1.);
#6509=VECTOR('',#22944,1.);
#6510=VECTOR('',#22947,1.);
#6511=VECTOR('',#22948,1.);
#6512=VECTOR('',#22949,1.);
#6513=VECTOR('',#22952,1.);
#6514=VECTOR('',#22953,1.);
#6515=VECTOR('',#22954,1.);
#6516=VECTOR('',#22957,1.);
#6517=VECTOR('',#22958,1.);
#6518=VECTOR('',#22959,1.);
#6519=VECTOR('',#22962,1.);
#6520=VECTOR('',#22963,1.);
#6521=VECTOR('',#22974,0.235);
#6522=VECTOR('',#22979,0.25);
#6523=VECTOR('',#22984,0.2125);
#7196=CIRCLE('',#18675,0.22);
#7197=CIRCLE('',#18677,0.24505);
#7198=CIRCLE('',#18679,0.24505);
#7199=CIRCLE('',#18681,0.175);
#8629=VERTEX_POINT('',#62361);
#8630=VERTEX_POINT('',#62362);
#8631=VERTEX_POINT('',#62364);
#8632=VERTEX_POINT('',#62366);
#8633=VERTEX_POINT('',#62370);
#8634=VERTEX_POINT('',#62372);
#8635=VERTEX_POINT('',#62376);
#8636=VERTEX_POINT('',#62378);
#8637=VERTEX_POINT('',#62382);
#8638=VERTEX_POINT('',#62384);
#8639=VERTEX_POINT('',#62388);
#8640=VERTEX_POINT('',#62390);
#8641=VERTEX_POINT('',#62398);
#8642=VERTEX_POINT('',#62401);
#8643=VERTEX_POINT('',#62405);
#8644=VERTEX_POINT('',#62409);
#10772=EDGE_CURVE('',#8629,#8630,#5371,.T.);
#10773=EDGE_CURVE('',#8629,#8631,#5372,.T.);
#10774=EDGE_CURVE('',#8631,#8632,#5373,.T.);
#10775=EDGE_CURVE('',#8630,#8632,#5374,.T.);
#10776=EDGE_CURVE('',#8633,#8629,#5375,.T.);
#10777=EDGE_CURVE('',#8633,#8634,#5376,.T.);
#10778=EDGE_CURVE('',#8634,#8631,#5377,.T.);
#10779=EDGE_CURVE('',#8635,#8633,#5378,.T.);
#10780=EDGE_CURVE('',#8635,#8636,#5379,.T.);
#10781=EDGE_CURVE('',#8636,#8634,#5380,.T.);
#10782=EDGE_CURVE('',#8637,#8635,#5381,.T.);
#10783=EDGE_CURVE('',#8637,#8638,#5382,.T.);
#10784=EDGE_CURVE('',#8638,#8636,#5383,.T.);
#10785=EDGE_CURVE('',#8639,#8637,#5384,.T.);
#10786=EDGE_CURVE('',#8639,#8640,#5385,.T.);
#10787=EDGE_CURVE('',#8640,#8638,#5386,.T.);
#10788=EDGE_CURVE('',#8630,#8639,#5387,.T.);
#10789=EDGE_CURVE('',#8632,#8640,#5388,.T.);
#10790=EDGE_CURVE('',#8641,#8641,#7196,.T.);
#10791=EDGE_CURVE('',#8642,#8642,#7197,.T.);
#10792=EDGE_CURVE('',#8642,#8641,#5389,.T.);
#10793=EDGE_CURVE('',#8643,#8643,#7198,.F.);
#10794=EDGE_CURVE('',#8643,#8642,#5390,.T.);
#10795=EDGE_CURVE('',#8644,#8644,#7199,.T.);
#10796=EDGE_CURVE('',#8644,#8643,#5391,.T.);
#15041=ORIENTED_EDGE('',*,*,#10772,.F.);
#15042=ORIENTED_EDGE('',*,*,#10773,.T.);
#15043=ORIENTED_EDGE('',*,*,#10774,.T.);
#15044=ORIENTED_EDGE('',*,*,#10775,.F.);
#15045=ORIENTED_EDGE('',*,*,#10776,.F.);
#15046=ORIENTED_EDGE('',*,*,#10777,.T.);
#15047=ORIENTED_EDGE('',*,*,#10778,.T.);
#15048=ORIENTED_EDGE('',*,*,#10773,.F.);
#15049=ORIENTED_EDGE('',*,*,#10779,.F.);
#15050=ORIENTED_EDGE('',*,*,#10780,.T.);
#15051=ORIENTED_EDGE('',*,*,#10781,.T.);
#15052=ORIENTED_EDGE('',*,*,#10777,.F.);
#15053=ORIENTED_EDGE('',*,*,#10782,.F.);
#15054=ORIENTED_EDGE('',*,*,#10783,.T.);
#15055=ORIENTED_EDGE('',*,*,#10784,.T.);
#15056=ORIENTED_EDGE('',*,*,#10780,.F.);
#15057=ORIENTED_EDGE('',*,*,#10785,.F.);
#15058=ORIENTED_EDGE('',*,*,#10786,.T.);
#15059=ORIENTED_EDGE('',*,*,#10787,.T.);
#15060=ORIENTED_EDGE('',*,*,#10783,.F.);
#15061=ORIENTED_EDGE('',*,*,#10788,.F.);
#15062=ORIENTED_EDGE('',*,*,#10775,.T.);
#15063=ORIENTED_EDGE('',*,*,#10789,.T.);
#15064=ORIENTED_EDGE('',*,*,#10786,.F.);
#15065=ORIENTED_EDGE('',*,*,#10789,.F.);
#15066=ORIENTED_EDGE('',*,*,#10774,.F.);
#15067=ORIENTED_EDGE('',*,*,#10778,.F.);
#15068=ORIENTED_EDGE('',*,*,#10781,.F.);
#15069=ORIENTED_EDGE('',*,*,#10784,.F.);
#15070=ORIENTED_EDGE('',*,*,#10787,.F.);
#15071=ORIENTED_EDGE('',*,*,#10790,.F.);
#15072=ORIENTED_EDGE('',*,*,#10772,.T.);
#15073=ORIENTED_EDGE('',*,*,#10788,.T.);
#15074=ORIENTED_EDGE('',*,*,#10785,.T.);
#15075=ORIENTED_EDGE('',*,*,#10782,.T.);
#15076=ORIENTED_EDGE('',*,*,#10779,.T.);
#15077=ORIENTED_EDGE('',*,*,#10776,.T.);
#15078=ORIENTED_EDGE('',*,*,#10791,.F.);
#15079=ORIENTED_EDGE('',*,*,#10792,.T.);
#15080=ORIENTED_EDGE('',*,*,#10790,.T.);
#15081=ORIENTED_EDGE('',*,*,#10792,.F.);
#15082=ORIENTED_EDGE('',*,*,#10793,.F.);
#15083=ORIENTED_EDGE('',*,*,#10794,.T.);
#15084=ORIENTED_EDGE('',*,*,#10791,.T.);
#15085=ORIENTED_EDGE('',*,*,#10794,.F.);
#15086=ORIENTED_EDGE('',*,*,#10795,.F.);
#15087=ORIENTED_EDGE('',*,*,#10796,.T.);
#15088=ORIENTED_EDGE('',*,*,#10793,.T.);
#15089=ORIENTED_EDGE('',*,*,#10796,.F.);
#15090=ORIENTED_EDGE('',*,*,#10795,.T.);
#15428=CYLINDRICAL_SURFACE('',#18678,0.24505);
#16336=ADVANCED_FACE('',(#3026),#2101,.F.);
#16337=ADVANCED_FACE('',(#3027),#2102,.F.);
#16338=ADVANCED_FACE('',(#3028),#2103,.F.);
#16339=ADVANCED_FACE('',(#3029),#2104,.F.);
#16340=ADVANCED_FACE('',(#3030),#2105,.F.);
#16341=ADVANCED_FACE('',(#3031),#2106,.F.);
#16342=ADVANCED_FACE('',(#3032),#2107,.F.);
#16343=ADVANCED_FACE('',(#3033,#1629),#2108,.T.);
#16344=ADVANCED_FACE('',(#3034),#1045,.T.);
#16345=ADVANCED_FACE('',(#3035),#15428,.T.);
#16346=ADVANCED_FACE('',(#3036),#1046,.T.);
#16347=ADVANCED_FACE('',(#3037),#2109,.T.);
#16449=CLOSED_SHELL('',(#16336,#16337,#16338,#16339,#16340,#16341,#16342,
#16343,#16344,#16345,#16346,#16347));
#18666=AXIS2_PLACEMENT_3D('',#62359,#22932,#22933);
#18667=AXIS2_PLACEMENT_3D('',#62360,#22934,#22935);
#18668=AXIS2_PLACEMENT_3D('',#62369,#22940,#22941);
#18669=AXIS2_PLACEMENT_3D('',#62375,#22945,#22946);
#18670=AXIS2_PLACEMENT_3D('',#62381,#22950,#22951);
#18671=AXIS2_PLACEMENT_3D('',#62387,#22955,#22956);
#18672=AXIS2_PLACEMENT_3D('',#62393,#22960,#22961);
#18673=AXIS2_PLACEMENT_3D('',#62396,#22964,#22965);
#18674=AXIS2_PLACEMENT_3D('',#62397,#22966,#22967);
#18675=AXIS2_PLACEMENT_3D('',#62399,#22968,#22969);
#18676=AXIS2_PLACEMENT_3D('',#62400,#22970,#22971);
#18677=AXIS2_PLACEMENT_3D('',#62402,#22972,#22973);
#18678=AXIS2_PLACEMENT_3D('',#62404,#22975,#22976);
#18679=AXIS2_PLACEMENT_3D('',#62406,#22977,#22978);
#18680=AXIS2_PLACEMENT_3D('',#62408,#22980,#22981);
#18681=AXIS2_PLACEMENT_3D('',#62410,#22982,#22983);
#18682=AXIS2_PLACEMENT_3D('',#62412,#22985,#22986);
#22932=DIRECTION('axis',(0.,0.,1.));
#22933=DIRECTION('refdir',(1.,0.,0.));
#22934=DIRECTION('center_axis',(0.866025403784439,0.,-0.5));
#22935=DIRECTION('ref_axis',(0.5,0.,0.866025403784439));
#22936=DIRECTION('',(0.5,0.,0.866025403784439));
#22937=DIRECTION('',(0.,-1.,0.));
#22938=DIRECTION('',(0.5,0.,0.866025403784439));
#22939=DIRECTION('',(0.,-1.,0.));
#22940=DIRECTION('center_axis',(1.92296268638356E-16,0.,-1.));
#22941=DIRECTION('ref_axis',(1.,0.,1.92296268638356E-16));
#22942=DIRECTION('',(1.,0.,1.92296268638356E-16));
#22943=DIRECTION('',(0.,-1.,0.));
#22944=DIRECTION('',(1.,0.,1.92296268638356E-16));
#22945=DIRECTION('center_axis',(-0.866025403784439,0.,-0.5));
#22946=DIRECTION('ref_axis',(0.5,0.,-0.866025403784439));
#22947=DIRECTION('',(0.5,0.,-0.866025403784439));
#22948=DIRECTION('',(0.,-1.,0.));
#22949=DIRECTION('',(0.5,0.,-0.866025403784438));
#22950=DIRECTION('center_axis',(-0.866025403784439,0.,0.5));
#22951=DIRECTION('ref_axis',(-0.5,0.,-0.866025403784439));
#22952=DIRECTION('',(-0.5,0.,-0.866025403784439));
#22953=DIRECTION('',(0.,-1.,0.));
#22954=DIRECTION('',(-0.5,0.,-0.866025403784439));
#22955=DIRECTION('center_axis',(-1.92296268638356E-16,0.,1.));
#22956=DIRECTION('ref_axis',(-1.,0.,-1.92296268638356E-16));
#22957=DIRECTION('',(-1.,0.,-1.92296268638356E-16));
#22958=DIRECTION('',(0.,-1.,0.));
#22959=DIRECTION('',(-1.,0.,-1.92296268638356E-16));
#22960=DIRECTION('center_axis',(0.866025403784439,0.,0.5));
#22961=DIRECTION('ref_axis',(-0.5,0.,0.866025403784439));
#22962=DIRECTION('',(-0.5,0.,0.866025403784439));
#22963=DIRECTION('',(-0.5,0.,0.866025403784439));
#22964=DIRECTION('center_axis',(0.,-1.,0.));
#22965=DIRECTION('ref_axis',(0.,0.,-1.));
#22966=DIRECTION('center_axis',(0.,1.,0.));
#22967=DIRECTION('ref_axis',(0.,0.,1.));
#22968=DIRECTION('center_axis',(0.,-1.,0.));
#22969=DIRECTION('ref_axis',(1.,0.,0.));
#22970=DIRECTION('center_axis',(0.,-1.,0.));
#22971=DIRECTION('ref_axis',(1.,0.,0.));
#22972=DIRECTION('center_axis',(0.,-1.,0.));
#22973=DIRECTION('ref_axis',(1.,0.,0.));
#22974=DIRECTION('',(0.707106781186547,0.707106781186548,8.65956056235493E-17));
#22975=DIRECTION('center_axis',(0.,-1.,0.));
#22976=DIRECTION('ref_axis',(1.,0.,0.));
#22977=DIRECTION('center_axis',(0.,1.,0.));
#22978=DIRECTION('ref_axis',(1.,0.,0.));
#22979=DIRECTION('',(0.,1.,0.));
#22980=DIRECTION('center_axis',(0.,1.,0.));
#22981=DIRECTION('ref_axis',(1.,0.,0.));
#22982=DIRECTION('center_axis',(0.,-1.,0.));
#22983=DIRECTION('ref_axis',(1.,0.,0.));
#22984=DIRECTION('',(-0.707106781186547,0.707106781186548,-8.65956056235493E-17));
#22985=DIRECTION('center_axis',(0.,-1.,0.));
#22986=DIRECTION('ref_axis',(0.,0.,-1.));
#62359=CARTESIAN_POINT('',(0.,0.,0.));
#62360=CARTESIAN_POINT('Origin',(0.0721687836487032,0.,-0.125));
#62361=CARTESIAN_POINT('',(0.0721687836487032,0.,-0.125));
#62362=CARTESIAN_POINT('',(0.144337567297406,0.,0.));
#62363=CARTESIAN_POINT('',(0.117710979560879,0.,-0.0461186027918559));
#62364=CARTESIAN_POINT('',(0.0721687836487032,-0.25,-0.125));
#62365=CARTESIAN_POINT('',(0.0721687836487032,0.,-0.125));
#62366=CARTESIAN_POINT('',(0.144337567297406,-0.25,0.));
#62367=CARTESIAN_POINT('',(0.144337567297406,-0.25,0.));
#62368=CARTESIAN_POINT('',(0.144337567297406,0.,0.));
#62369=CARTESIAN_POINT('Origin',(-0.0721687836487032,0.,-0.125));
#62370=CARTESIAN_POINT('',(-0.0721687836487032,0.,-0.125));
#62371=CARTESIAN_POINT('',(0.0739156081756484,0.,-0.125));
#62372=CARTESIAN_POINT('',(-0.0721687836487032,-0.25,-0.125));
#62373=CARTESIAN_POINT('',(-0.0721687836487032,0.,-0.125));
#62374=CARTESIAN_POINT('',(0.0721687836487032,-0.25,-0.125));
#62375=CARTESIAN_POINT('Origin',(-0.144337567297406,0.,-4.16333634234434E-17));
#62376=CARTESIAN_POINT('',(-0.144337567297406,0.,-1.76762539787485E-17));
#62377=CARTESIAN_POINT('',(-0.0987953713852306,0.,-0.0788813972081442));
#62378=CARTESIAN_POINT('',(-0.144337567297406,-0.25,-2.77555756156289E-17));
#62379=CARTESIAN_POINT('',(-0.144337567297406,0.,-1.76762539787485E-17));
#62380=CARTESIAN_POINT('',(-0.0721687836487032,-0.25,-0.125));
#62381=CARTESIAN_POINT('Origin',(-0.0721687836487033,0.,0.125));
#62382=CARTESIAN_POINT('',(-0.0721687836487033,0.,0.125));
#62383=CARTESIAN_POINT('',(-0.0627109795608791,0.,0.141381397208144));
#62384=CARTESIAN_POINT('',(-0.0721687836487033,-0.25,0.125));
#62385=CARTESIAN_POINT('',(-0.0721687836487033,0.,0.125));
#62386=CARTESIAN_POINT('',(-0.144337567297406,-0.25,-1.76762539787485E-17));
#62387=CARTESIAN_POINT('Origin',(0.0721687836487032,0.,0.125));
#62388=CARTESIAN_POINT('',(0.0721687836487032,0.,0.125));
#62389=CARTESIAN_POINT('',(0.146084391824352,0.,0.125));
#62390=CARTESIAN_POINT('',(0.0721687836487032,-0.25,0.125));
#62391=CARTESIAN_POINT('',(0.0721687836487032,0.,0.125));
#62392=CARTESIAN_POINT('',(-0.0721687836487033,-0.25,0.125));
#62393=CARTESIAN_POINT('Origin',(0.144337567297406,0.,0.));
#62394=CARTESIAN_POINT('',(0.153795371385231,0.,-0.0163813972081441));
#62395=CARTESIAN_POINT('',(0.0721687836487032,-0.25,0.125));
#62396=CARTESIAN_POINT('Origin',(0.,-0.25,0.));
#62397=CARTESIAN_POINT('Origin',(0.22,0.,0.));
#62398=CARTESIAN_POINT('',(-0.22,-8.67361737988404E-18,-2.69422295812418E-17));
#62399=CARTESIAN_POINT('Origin',(0.,0.,0.));
#62400=CARTESIAN_POINT('Origin',(0.,-0.015,0.));
#62401=CARTESIAN_POINT('',(-0.24505,-0.02505,-3.00099698131059E-17));
#62402=CARTESIAN_POINT('Origin',(0.,-0.02505,0.));
#62403=CARTESIAN_POINT('',(-0.235,-0.015,-2.87791997799628E-17));
#62404=CARTESIAN_POINT('Origin',(0.,-0.3775,0.));
#62405=CARTESIAN_POINT('',(-0.24505,-0.72995,3.00099698131059E-17));
#62406=CARTESIAN_POINT('Origin',(0.,-0.72995,0.));
#62407=CARTESIAN_POINT('',(-0.24505,-0.3775,-3.00099698131059E-17));
#62408=CARTESIAN_POINT('Origin',(0.,-0.7625,0.));
#62409=CARTESIAN_POINT('',(-0.175,-0.8,-2.14313189850787E-17));
#62410=CARTESIAN_POINT('Origin',(0.,-0.8,0.));
#62411=CARTESIAN_POINT('',(-0.2125,-0.7625,-2.60237444818813E-17));
#62412=CARTESIAN_POINT('Origin',(0.,-0.8,0.));
#62680=UNCERTAINTY_MEASURE_WITH_UNIT(LENGTH_MEASURE(0.001),#62759,
'DISTANCE_ACCURACY_VALUE',
'Maximum model space distance between geometric entities at asserted c
onnectivities');
#62684=UNCERTAINTY_MEASURE_WITH_UNIT(LENGTH_MEASURE(0.001),#62759,
'DISTANCE_ACCURACY_VALUE',
'Maximum model space distance between geometric entities at asserted c
onnectivities');
#62754=(
GEOMETRIC_REPRESENTATION_CONTEXT(3)
GLOBAL_UNCERTAINTY_ASSIGNED_CONTEXT((#62680))
GLOBAL_UNIT_ASSIGNED_CONTEXT((#62759,#62761,#62762))
REPRESENTATION_CONTEXT('','3D')
);
#62758=(
GEOMETRIC_REPRESENTATION_CONTEXT(3)
GLOBAL_UNCERTAINTY_ASSIGNED_CONTEXT((#62684))
GLOBAL_UNIT_ASSIGNED_CONTEXT((#62759,#62761,#62762))
REPRESENTATION_CONTEXT('','3D')
);
#62759=(
LENGTH_UNIT()
NAMED_UNIT(*)
SI_UNIT(.CENTI.,.METRE.)
);
#62761=(
NAMED_UNIT(*)
PLANE_ANGLE_UNIT()
SI_UNIT($,.RADIAN.)
);
#62762=(
NAMED_UNIT(*)
SI_UNIT($,.STERADIAN.)
SOLID_ANGLE_UNIT()
);
#62832=SHAPE_DEFINITION_REPRESENTATION(#62915,#63100);
#62915=PRODUCT_DEFINITION_SHAPE('',$,#63174);
#63100=SHAPE_REPRESENTATION('',(#18666),#62754);
#63104=PRODUCT_DEFINITION_CONTEXT('part definition',#63325,'design');
#63174=PRODUCT_DEFINITION('Socket Set Screw - M5x8',
'Socket Set Screw - M5x8',#63247,#63104);
#63247=PRODUCT_DEFINITION_FORMATION('',$,#63396);
#63325=APPLICATION_CONTEXT(
'Core Data for Automotive Mechanical Design Process');
#63326=PRODUCT_CONTEXT('part definition',#63325,'mechanical');
#63396=PRODUCT('Socket Set Screw - M5x8','Socket Set Screw - M5x8',
'Socket Set Screw - M5x8',(#63326));
#63463=COLOUR_RGB('Black',0.12,0.14,0.17);
#63464=FILL_AREA_STYLE_COLOUR('',#63463);
#63465=FILL_AREA_STYLE('',(#63464));
#63466=SURFACE_STYLE_FILL_AREA(#63465);
#63467=SURFACE_SIDE_STYLE('',(#63466));
#63468=SURFACE_STYLE_USAGE(.BOTH.,#63467);
#63469=PRESENTATION_STYLE_ASSIGNMENT((#63468));
ENDSEC;
END-ISO-10303-21;
